ISO-10303-21;
HEADER;
FILE_DESCRIPTION (('STEP AP214'),
    '1' );
FILE_NAME ('shaft1.step',
    '2026-09-28T15:49:00',
    ( '' ),
    ( '' ),
    'SwSTEP 2.0',
    'SolidWorks 2026',
    '' );
FILE_SCHEMA (( 'AUTOMOTIVE_DESIGN' ));
ENDSEC;

DATA;
#12=( NAMED_UNIT ( * ) SI_UNIT ( $, .STERADIAN. ) SOLID_ANGLE_UNIT ( ) );
#18=VECTOR ( 'NONE', #20974, 1000.000000000000000 ) ;
#39=ADVANCED_BREP_SHAPE_REPRESENTATION ( '', ( #22133, #21307 ), #32890 ) ;
#58=ORIENTED_EDGE ( 'NONE', *, *, #8163, .F. ) ;
#81=CARTESIAN_POINT ( 'NONE',  ( 0.000000000000000000, 0.000000000000000000, -33.50000000000000711 ) ) ;
#87=DIRECTION ( 'NONE',  ( 0.000000000000000000, 0.000000000000000000, -1.000000000000000000 ) ) ;
#114=CIRCLE ( 'NONE', #34046, 4.000000000000000000 ) ;
#120=CARTESIAN_POINT ( 'NONE',  ( 0.000000000000000000, 0.000000000000000000, -50.00000000000000000 ) ) ;
#123=ORIENTED_EDGE ( 'NONE', *, *, #11203, .T. ) ;
#187=VECTOR ( 'NONE', #26891, 1000.000000000000000 ) ;
#222=ORIENTED_EDGE ( 'NONE', *, *, #22015, .T. ) ;
#292=DIRECTION ( 'NONE',  ( -1.000000000000000000, 0.000000000000000000, 0.000000000000000000 ) ) ;
#304=EDGE_CURVE ( 'NONE', #15866, #20180, #29503, .T. ) ;
#316=CARTESIAN_POINT ( 'NONE',  ( -4.000000000000000000, 0.000000000000000000, 55.00000000000000000 ) ) ;
#347=CARTESIAN_POINT ( 'NONE',  ( 0.000000000000000000, 0.000000000000000000, 49.10000000000000142 ) ) ;
#373=DIRECTION ( 'NONE',  ( 0.000000000000000000, 0.000000000000000000, 1.000000000000000000 ) ) ;
#473=FACE_BOUND ( 'NONE', #33922, .T. ) ;
#485=VERTEX_POINT ( 'NONE', #11755 ) ;
#498=SHAPE_DEFINITION_REPRESENTATION ( #31065, #33742 ) ;
#499=CYLINDRICAL_SURFACE ( 'NONE', #3569, 3.799999999999999822 ) ;
#522=EDGE_CURVE ( 'NONE', #24075, #10339, #11416, .T. ) ;
#589=CARTESIAN_POINT ( 'NONE',  ( -3.799999999999999822, 0.000000000000000000, -34.40000000000000568 ) ) ;
#644=DIRECTION ( 'NONE',  ( -1.000000000000000000, 0.000000000000000000, 0.000000000000000000 ) ) ;
#761=PRODUCT_DEFINITION_CONTEXT ( 'detailed design', #16046, 'design' ) ;
#845=ORIENTED_EDGE ( 'NONE', *, *, #12218, .T. ) ;
#961=EDGE_CURVE ( 'NONE', #25611, #15981, #4752, .T. ) ;
#1004=DIRECTION ( 'NONE',  ( 0.000000000000000000, 0.000000000000000000, 1.000000000000000000 ) ) ;
#1006=UNCERTAINTY_MEASURE_WITH_UNIT (LENGTH_MEASURE( 1.000000000000000082E-05 ), #14051, 'distance_accuracy_value', 'NONE');
#1126=AXIS2_PLACEMENT_3D ( 'NONE', #27961, #30662, #22899 ) ;
#1132=DIRECTION ( 'NONE',  ( -1.000000000000000000, 0.000000000000000000, 0.000000000000000000 ) ) ;
#1138=EDGE_CURVE ( 'NONE', #15981, #31617, #31232, .T. ) ;
#1217=LINE ( 'NONE', #29120, #16781 ) ;
#1224=DIRECTION ( 'NONE',  ( -1.000000000000000000, 0.000000000000000000, 0.000000000000000000 ) ) ;
#1279=CARTESIAN_POINT ( 'NONE',  ( 3.799999999999999822, 0.000000000000000000, 49.10000000000000142 ) ) ;
#1380=EDGE_CURVE ( 'NONE', #24945, #10090, #3111, .T. ) ;
#1389=EDGE_LOOP ( 'NONE', ( #12090, #20252 ) ) ;
#1505=MECHANICAL_DESIGN_GEOMETRIC_PRESENTATION_REPRESENTATION('',(#15878),#35441);
#1508=VECTOR ( 'NONE', #30904, 1000.000000000000000 ) ;
#1644=CARTESIAN_POINT ( 'NONE',  ( -3.799999999999999822, 4.653657836759942730E-16, 49.10000000000000142 ) ) ;
#1684=DIRECTION ( 'NONE',  ( 0.000000000000000000, 0.000000000000000000, -1.000000000000000000 ) ) ;
#1692=CIRCLE ( 'NONE', #1126, 4.000000000000000000 ) ;
#1777=EDGE_CURVE ( 'NONE', #11644, #9824, #8275, .T. ) ;
#1782=FACE_OUTER_BOUND ( 'NONE', #25598, .T. ) ;
#1787=EDGE_CURVE ( 'NONE', #16603, #25611, #17470, .T. ) ;
#1821=VECTOR ( 'NONE', #34895, 1000.000000000000000 ) ;
#1852=CARTESIAN_POINT ( 'NONE',  ( 0.000000000000000000, 0.000000000000000000, -39.50000000000000711 ) ) ;
#1870=DIRECTION ( 'NONE',  ( -1.000000000000000000, 0.000000000000000000, 0.000000000000000000 ) ) ;
#1894=CARTESIAN_POINT ( 'NONE',  ( 0.000000000000000000, 0.000000000000000000, -55.00000000000000000 ) ) ;
#1999=EDGE_LOOP ( 'NONE', ( #25556, #11854, #21246, #31123 ) ) ;
#2061=ORIENTED_EDGE ( 'NONE', *, *, #29229, .T. ) ;
#2079=DIRECTION ( 'NONE',  ( -1.000000000000000000, 0.000000000000000000, 0.000000000000000000 ) ) ;
#2081=LINE ( 'NONE', #13061, #11372 ) ;
#2201=EDGE_LOOP ( 'NONE', ( #10508, #26216 ) ) ;
#2287=EDGE_LOOP ( 'NONE', ( #13173, #12637, #23366, #24486 ) ) ;
#2354=CARTESIAN_POINT ( 'NONE',  ( 0.000000000000000000, 0.000000000000000000, -40.40000000000000568 ) ) ;
#2398=DIRECTION ( 'NONE',  ( 0.000000000000000000, 0.000000000000000000, -1.000000000000000000 ) ) ;
#2421=DIRECTION ( 'NONE',  ( 0.000000000000000000, 0.000000000000000000, -1.000000000000000000 ) ) ;
#2579=CARTESIAN_POINT ( 'NONE',  ( -3.799999999999999822, 4.653657836759942730E-16, 49.10000000000000142 ) ) ;
#2608=CARTESIAN_POINT ( 'NONE',  ( -3.799999999999999822, 0.000000000000000000, -33.50000000000000711 ) ) ;
#2742=( NAMED_UNIT ( * ) SI_UNIT ( $, .STERADIAN. ) SOLID_ANGLE_UNIT ( ) );
#2816=CARTESIAN_POINT ( 'NONE',  ( 0.000000000000000000, 0.000000000000000000, -34.40000000000000568 ) ) ;
#2869=DIRECTION ( 'NONE',  ( -1.000000000000000000, 0.000000000000000000, 0.000000000000000000 ) ) ;
#2889=ORIENTED_EDGE ( 'NONE', *, *, #10154, .F. ) ;
#2917=AXIS2_PLACEMENT_3D ( 'NONE', #2816, #87, #29987 ) ;
#2922=DIRECTION ( 'NONE',  ( 0.000000000000000000, 0.000000000000000000, -1.000000000000000000 ) ) ;
#2951=VERTEX_POINT ( 'NONE', #4590 ) ;
#2975=ORIENTED_EDGE ( 'NONE', *, *, #1380, .T. ) ;
#3098=DIRECTION ( 'NONE',  ( 1.000000000000000000, 0.000000000000000000, 0.000000000000000000 ) ) ;
#3111=CIRCLE ( 'NONE', #19738, 4.000000000000000000 ) ;
#3129=PRODUCT_DEFINITION ( 'UNKNOWN', '', #8615, #761 ) ;
#3180=DIRECTION ( 'NONE',  ( 1.000000000000000000, 0.000000000000000000, 0.000000000000000000 ) ) ;
#3338=VERTEX_POINT ( 'NONE', #21799 ) ;
#3392=CARTESIAN_POINT ( 'NONE',  ( 0.000000000000000000, 0.000000000000000000, -39.50000000000000711 ) ) ;
#3544=ORIENTED_EDGE ( 'NONE', *, *, #26796, .T. ) ;
#3569=AXIS2_PLACEMENT_3D ( 'NONE', #16328, #24815, #2869 ) ;
#3702=CARTESIAN_POINT ( 'NONE',  ( -4.000000000000000000, 0.000000000000000000, -40.40000000000000568 ) ) ;
#3750=CIRCLE ( 'NONE', #30774, 4.000000000000000000 ) ;
#3789=EDGE_CURVE ( 'NONE', #19841, #8832, #24896, .T. ) ;
#3814=DIRECTION ( 'NONE',  ( -1.000000000000000000, 0.000000000000000000, 0.000000000000000000 ) ) ;
#3823=CIRCLE ( 'NONE', #14715, 4.000000000000000000 ) ;
#3834=ORIENTED_EDGE ( 'NONE', *, *, #26246, .F. ) ;
#3952=CARTESIAN_POINT ( 'NONE',  ( 0.000000000000000000, 0.000000000000000000, 49.10000000000000142 ) ) ;
#3964=EDGE_LOOP ( 'NONE', ( #35428, #3544 ) ) ;
#3989=VERTEX_POINT ( 'NONE', #14928 ) ;
#4167=CARTESIAN_POINT ( 'NONE',  ( 0.000000000000000000, 0.000000000000000000, 55.00000000000000000 ) ) ;
#4311=CARTESIAN_POINT ( 'NONE',  ( 3.799999999999999822, 4.653657836759942730E-16, -49.10000000000000142 ) ) ;
#4318=AXIS2_PLACEMENT_3D ( 'NONE', #3952, #23002, #17414 ) ;
#4343=CIRCLE ( 'NONE', #29053, 4.000000000000000000 ) ;
#4393=PLANE ( 'NONE',  #10413 ) ;
#4400=EDGE_LOOP ( 'NONE', ( #17520, #32699, #15268, #30435 ) ) ;
#4501=CARTESIAN_POINT ( 'NONE',  ( 0.000000000000000000, 0.000000000000000000, 55.00000000000000000 ) ) ;
#4515=ORIENTED_EDGE ( 'NONE', *, *, #1138, .F. ) ;
#4590=CARTESIAN_POINT ( 'NONE',  ( -3.799999999999999822, 0.000000000000000000, -49.10000000000000142 ) ) ;
#4655=CARTESIAN_POINT ( 'NONE',  ( 4.000000000000000000, 4.898587196589412829E-16, 55.00000000000000000 ) ) ;
#4675=ORIENTED_EDGE ( 'NONE', *, *, #7522, .T. ) ;
#4676=LINE ( 'NONE', #4311, #13705 ) ;
#4752=LINE ( 'NONE', #10317, #187 ) ;
#4756=DIRECTION ( 'NONE',  ( 0.000000000000000000, 0.000000000000000000, 1.000000000000000000 ) ) ;
#4818=DIRECTION ( 'NONE',  ( 0.000000000000000000, 0.000000000000000000, -1.000000000000000000 ) ) ;
#4838=FACE_BOUND ( 'NONE', #2201, .T. ) ;
#4870=EDGE_CURVE ( 'NONE', #27386, #20308, #12918, .T. ) ;
#5034=VECTOR ( 'NONE', #33715, 1000.000000000000000 ) ;
#5125=EDGE_LOOP ( 'NONE', ( #27947, #16717, #4515, #11775 ) ) ;
#5298=EDGE_LOOP ( 'NONE', ( #28096, #24123 ) ) ;
#5308=CARTESIAN_POINT ( 'NONE',  ( 0.000000000000000000, 0.000000000000000000, -40.40000000000000568 ) ) ;
#5482=ADVANCED_FACE ( 'NONE', ( #6621, #15067 ), #17951, .F. ) ;
#5582=DIRECTION ( 'NONE',  ( 0.000000000000000000, 0.000000000000000000, -1.000000000000000000 ) ) ;
#5596=FACE_OUTER_BOUND ( 'NONE', #11254, .T. ) ;
#5618=ADVANCED_FACE ( 'NONE', ( #18494 ), #8044, .T. ) ;
#5631=CIRCLE ( 'NONE', #25755, 3.799999999999999822 ) ;
#5658=CARTESIAN_POINT ( 'NONE',  ( -4.000000000000000000, 0.000000000000000000, 55.00000000000000000 ) ) ;
#5662=LINE ( 'NONE', #33198, #25645 ) ;
#5671=CARTESIAN_POINT ( 'NONE',  ( 4.000000000000000000, 4.898587196589412829E-16, 55.00000000000000000 ) ) ;
#5690=FACE_OUTER_BOUND ( 'NONE', #25878, .T. ) ;
#5719=ORIENTED_EDGE ( 'NONE', *, *, #12415, .F. ) ;
#5724=DIRECTION ( 'NONE',  ( 0.000000000000000000, 0.000000000000000000, -1.000000000000000000 ) ) ;
#5737=DIRECTION ( 'NONE',  ( -1.000000000000000000, 0.000000000000000000, 0.000000000000000000 ) ) ;
#5754=CYLINDRICAL_SURFACE ( 'NONE', #16417, 4.000000000000000000 ) ;
#5784=EDGE_CURVE ( 'NONE', #34725, #3338, #21549, .T. ) ;
#5792=PLANE ( 'NONE',  #29704 ) ;
#5815=ADVANCED_FACE ( 'NONE', ( #473, #30380 ), #13629, .F. ) ;
#5868=CARTESIAN_POINT ( 'NONE',  ( 0.000000000000000000, 0.000000000000000000, 49.10000000000000142 ) ) ;
#5872=FACE_OUTER_BOUND ( 'NONE', #11812, .T. ) ;
#5959=FILL_AREA_STYLE ('',( #30284 ) ) ;
#5964=EDGE_CURVE ( 'NONE', #10090, #24945, #4343, .T. ) ;
#6030=AXIS2_PLACEMENT_3D ( 'NONE', #12391, #23193, #6452 ) ;
#6178=LINE ( 'NONE', #17141, #5034 ) ;
#6284=CYLINDRICAL_SURFACE ( 'NONE', #30360, 4.000000000000000000 ) ;
#6296=ORIENTED_EDGE ( 'NONE', *, *, #9986, .F. ) ;
#6306=ADVANCED_FACE ( 'NONE', ( #32160 ), #7316, .T. ) ;
#6400=DIRECTION ( 'NONE',  ( 0.000000000000000000, 0.000000000000000000, -1.000000000000000000 ) ) ;
#6452=DIRECTION ( 'NONE',  ( -1.000000000000000000, 0.000000000000000000, 0.000000000000000000 ) ) ;
#6555=EDGE_CURVE ( 'NONE', #33826, #7350, #3823, .T. ) ;
#6591=CARTESIAN_POINT ( 'NONE',  ( 4.000000000000000000, 4.898587196589412829E-16, -34.40000000000000568 ) ) ;
#6600=DIRECTION ( 'NONE',  ( 0.000000000000000000, 0.000000000000000000, -1.000000000000000000 ) ) ;
#6616=CARTESIAN_POINT ( 'NONE',  ( 4.000000000000000000, 4.898587196589412829E-16, -40.40000000000000568 ) ) ;
#6617=EDGE_CURVE ( 'NONE', #20180, #15866, #9539, .T. ) ;
#6621=FACE_OUTER_BOUND ( 'NONE', #22618, .T. ) ;
#6812=DIRECTION ( 'NONE',  ( 0.000000000000000000, 0.000000000000000000, -1.000000000000000000 ) ) ;
#6825=EDGE_CURVE ( 'NONE', #20308, #27386, #13025, .T. ) ;
#6925=ADVANCED_FACE ( 'NONE', ( #9018 ), #33871, .T. ) ;
#6986=ORIENTED_EDGE ( 'NONE', *, *, #10768, .F. ) ;
#7074=DIRECTION ( 'NONE',  ( -1.000000000000000000, 0.000000000000000000, 0.000000000000000000 ) ) ;
#7179=ORIENTED_EDGE ( 'NONE', *, *, #7522, .F. ) ;
#7293=VECTOR ( 'NONE', #16630, 1000.000000000000000 ) ;
#7316=CYLINDRICAL_SURFACE ( 'NONE', #23031, 3.799999999999999822 ) ;
#7331=AXIS2_PLACEMENT_3D ( 'NONE', #35603, #18847, #30373 ) ;
#7350=VERTEX_POINT ( 'NONE', #19712 ) ;
#7513=CARTESIAN_POINT ( 'NONE',  ( 0.000000000000000000, 0.000000000000000000, -39.50000000000000711 ) ) ;
#7522=EDGE_CURVE ( 'NONE', #24075, #30211, #16492, .T. ) ;
#7530=ORIENTED_EDGE ( 'NONE', *, *, #8163, .T. ) ;
#7589=AXIS2_PLACEMENT_3D ( 'NONE', #8026, #11094, #16288 ) ;
#7667=EDGE_LOOP ( 'NONE', ( #28272, #29649, #16088, #26662 ) ) ;
#7700=CARTESIAN_POINT ( 'NONE',  ( 0.000000000000000000, 0.000000000000000000, 49.10000000000000142 ) ) ;
#7710=EDGE_CURVE ( 'NONE', #15866, #29572, #6178, .T. ) ;
#7728=ORIENTED_EDGE ( 'NONE', *, *, #20623, .F. ) ;
#7753=EDGE_LOOP ( 'NONE', ( #7179, #6986 ) ) ;
#7770=ORIENTED_EDGE ( 'NONE', *, *, #5964, .F. ) ;
#7783=CARTESIAN_POINT ( 'NONE',  ( -4.000000000000000000, 0.000000000000000000, 50.00000000000000000 ) ) ;
#7800=LINE ( 'NONE', #30132, #22312 ) ;
#7868=CARTESIAN_POINT ( 'NONE',  ( 0.000000000000000000, 0.000000000000000000, -34.40000000000000568 ) ) ;
#7896=CIRCLE ( 'NONE', #29205, 3.799999999999999822 ) ;
#7933=ORIENTED_EDGE ( 'NONE', *, *, #34608, .T. ) ;
#8026=CARTESIAN_POINT ( 'NONE',  ( 0.000000000000000000, 0.000000000000000000, 49.10000000000000142 ) ) ;
#8042=PLANE ( 'NONE',  #28773 ) ;
#8044=CYLINDRICAL_SURFACE ( 'NONE', #31922, 3.799999999999999822 ) ;
#8163=EDGE_CURVE ( 'NONE', #19841, #26766, #2081, .T. ) ;
#8180=CIRCLE ( 'NONE', #7589, 3.799999999999999822 ) ;
#8215=CARTESIAN_POINT ( 'NONE',  ( 0.000000000000000000, 0.000000000000000000, -55.00000000000000000 ) ) ;
#8260=AXIS2_PLACEMENT_3D ( 'NONE', #3392, #5724, #10953 ) ;
#8275=CIRCLE ( 'NONE', #10006, 3.799999999999999822 ) ;
#8346=DIRECTION ( 'NONE',  ( 0.000000000000000000, 0.000000000000000000, -1.000000000000000000 ) ) ;
#8423=CARTESIAN_POINT ( 'NONE',  ( 0.000000000000000000, 0.000000000000000000, 55.00000000000000000 ) ) ;
#8448=CIRCLE ( 'NONE', #25705, 4.000000000000000000 ) ;
#8473=ORIENTED_EDGE ( 'NONE', *, *, #12415, .T. ) ;
#8485=FACE_OUTER_BOUND ( 'NONE', #5298, .T. ) ;
#8515=CARTESIAN_POINT ( 'NONE',  ( 3.799999999999999822, 4.653657836759942730E-16, -49.10000000000000142 ) ) ;
#8614=AXIS2_PLACEMENT_3D ( 'NONE', #26035, #17737, #644 ) ;
#8615=PRODUCT_DEFINITION_FORMATION_WITH_SPECIFIED_SOURCE ( 'ANY', '', #18142, .NOT_KNOWN. ) ;
#8634=( NAMED_UNIT ( * ) PLANE_ANGLE_UNIT ( ) SI_UNIT ( $, .RADIAN. ) );
#8644=ORIENTED_EDGE ( 'NONE', *, *, #35432, .F. ) ;
#8680=VERTEX_POINT ( 'NONE', #12208 ) ;
#8741=CARTESIAN_POINT ( 'NONE',  ( 4.000000000000000000, 4.898587196589412829E-16, 55.00000000000000000 ) ) ;
#8744=ORIENTED_EDGE ( 'NONE', *, *, #1787, .F. ) ;
#8759=PRODUCT_CONTEXT ( 'NONE', #14221, 'mechanical' ) ;
#8832=VERTEX_POINT ( 'NONE', #6616 ) ;
#8908=CYLINDRICAL_SURFACE ( 'NONE', #23751, 3.799999999999999822 ) ;
#8983=( LENGTH_UNIT ( ) NAMED_UNIT ( * ) SI_UNIT ( .MILLI., .METRE. ) );
#9018=FACE_OUTER_BOUND ( 'NONE', #9903, .T. ) ;
#9045=ORIENTED_EDGE ( 'NONE', *, *, #26246, .T. ) ;
#9087=ADVANCED_FACE ( 'NONE', ( #5872 ), #19535, .T. ) ;
#9189=CARTESIAN_POINT ( 'NONE',  ( 0.000000000000000000, 0.000000000000000000, 55.00000000000000000 ) ) ;
#9194=DIRECTION ( 'NONE',  ( -1.000000000000000000, 0.000000000000000000, 0.000000000000000000 ) ) ;
#9247=CARTESIAN_POINT ( 'NONE',  ( 0.000000000000000000, 0.000000000000000000, -50.00000000000000000 ) ) ;
#9367=DIRECTION ( 'NONE',  ( -1.000000000000000000, 0.000000000000000000, 0.000000000000000000 ) ) ;
#9482=ORIENTED_EDGE ( 'NONE', *, *, #3789, .F. ) ;
#9539=CIRCLE ( 'NONE', #11294, 3.799999999999999822 ) ;
#9558=CARTESIAN_POINT ( 'NONE',  ( 0.000000000000000000, 0.000000000000000000, 55.00000000000000000 ) ) ;
#9607=CARTESIAN_POINT ( 'NONE',  ( 4.000000000000000000, 4.898587196589412829E-16, -33.50000000000000711 ) ) ;
#9644=CARTESIAN_POINT ( 'NONE',  ( 0.000000000000000000, 0.000000000000000000, -50.00000000000000000 ) ) ;
#9662=DIRECTION ( 'NONE',  ( 0.000000000000000000, 0.000000000000000000, -1.000000000000000000 ) ) ;
#9674=EDGE_LOOP ( 'NONE', ( #3834, #24246, #7530, #28727 ) ) ;
#9781=FACE_OUTER_BOUND ( 'NONE', #18117, .T. ) ;
#9824=VERTEX_POINT ( 'NONE', #2579 ) ;
#9832=CARTESIAN_POINT ( 'NONE',  ( 0.000000000000000000, 0.000000000000000000, 55.00000000000000000 ) ) ;
#9899=ORIENTED_EDGE ( 'NONE', *, *, #18522, .F. ) ;
#9903=EDGE_LOOP ( 'NONE', ( #19724, #2975, #23589, #123 ) ) ;
#9945=CIRCLE ( 'NONE', #31791, 4.000000000000000000 ) ;
#9986=EDGE_CURVE ( 'NONE', #27576, #485, #33325, .T. ) ;
#10006=AXIS2_PLACEMENT_3D ( 'NONE', #347, #11343, #19594 ) ;
#10055=DIRECTION ( 'NONE',  ( 0.000000000000000000, 0.000000000000000000, 1.000000000000000000 ) ) ;
#10090=VERTEX_POINT ( 'NONE', #19977 ) ;
#10154=EDGE_CURVE ( 'NONE', #10339, #8680, #14910, .T. ) ;
#10297=PLANE ( 'NONE',  #24780 ) ;
#10307=DIRECTION ( 'NONE',  ( -1.000000000000000000, 0.000000000000000000, 0.000000000000000000 ) ) ;
#10317=CARTESIAN_POINT ( 'NONE',  ( -3.799999999999999822, 0.000000000000000000, -39.50000000000000711 ) ) ;
#10339=VERTEX_POINT ( 'NONE', #33252 ) ;
#10395=ADVANCED_FACE ( 'NONE', ( #20068 ), #25685, .T. ) ;
#10413=AXIS2_PLACEMENT_3D ( 'NONE', #12847, #31741, #7074 ) ;
#10444=DIRECTION ( 'NONE',  ( 0.000000000000000000, 0.000000000000000000, -1.000000000000000000 ) ) ;
#10471=DIRECTION ( 'NONE',  ( 0.000000000000000000, 0.000000000000000000, -1.000000000000000000 ) ) ;
#10507=DIRECTION ( 'NONE',  ( -1.000000000000000000, 0.000000000000000000, 0.000000000000000000 ) ) ;
#10508=ORIENTED_EDGE ( 'NONE', *, *, #1138, .T. ) ;
#10638=VECTOR ( 'NONE', #12622, 1000.000000000000000 ) ;
#10732=FACE_BOUND ( 'NONE', #1389, .T. ) ;
#10768=EDGE_CURVE ( 'NONE', #30211, #24075, #14391, .T. ) ;
#10941=DIRECTION ( 'NONE',  ( 0.000000000000000000, 0.000000000000000000, -1.000000000000000000 ) ) ;
#10953=DIRECTION ( 'NONE',  ( -1.000000000000000000, 0.000000000000000000, 0.000000000000000000 ) ) ;
#10958=VERTEX_POINT ( 'NONE', #20201 ) ;
#10960=CIRCLE ( 'NONE', #31079, 4.000000000000000000 ) ;
#10971=AXIS2_PLACEMENT_3D ( 'NONE', #18411, #4756, #15699 ) ;
#10991=DIRECTION ( 'NONE',  ( 0.000000000000000000, 0.000000000000000000, -1.000000000000000000 ) ) ;
#11017=( NAMED_UNIT ( * ) SI_UNIT ( $, .STERADIAN. ) SOLID_ANGLE_UNIT ( ) );
#11071=LINE ( 'NONE', #22040, #33740 ) ;
#11094=DIRECTION ( 'NONE',  ( 0.000000000000000000, 0.000000000000000000, -1.000000000000000000 ) ) ;
#11102=ADVANCED_FACE ( 'NONE', ( #9781, #23272 ), #4393, .T. ) ;
#11175=ADVANCED_FACE ( 'NONE', ( #25994 ), #23650, .T. ) ;
#11203=EDGE_CURVE ( 'NONE', #24596, #17756, #27093, .T. ) ;
#11254=EDGE_LOOP ( 'NONE', ( #13848, #13986, #222, #19449 ) ) ;
#11281=ADVANCED_FACE ( 'NONE', ( #24183 ), #30115, .T. ) ;
#11294=AXIS2_PLACEMENT_3D ( 'NONE', #23825, #1684, #29767 ) ;
#11343=DIRECTION ( 'NONE',  ( 0.000000000000000000, 0.000000000000000000, -1.000000000000000000 ) ) ;
#11346=CARTESIAN_POINT ( 'NONE',  ( 0.000000000000000000, 0.000000000000000000, 55.00000000000000000 ) ) ;
#11347=AXIS2_PLACEMENT_3D ( 'NONE', #13574, #24741, #2079 ) ;
#11372=VECTOR ( 'NONE', #21803, 1000.000000000000000 ) ;
#11416=LINE ( 'NONE', #27811, #31768 ) ;
#11472=FACE_OUTER_BOUND ( 'NONE', #3964, .T. ) ;
#11513=DIRECTION ( 'NONE',  ( 0.000000000000000000, 0.000000000000000000, -1.000000000000000000 ) ) ;
#11644=VERTEX_POINT ( 'NONE', #1279 ) ;
#11652=CIRCLE ( 'NONE', #29491, 4.000000000000000000 ) ;
#11693=AXIS2_PLACEMENT_3D ( 'NONE', #14058, #22873, #19794 ) ;
#11725=ORIENTED_EDGE ( 'NONE', *, *, #7710, .T. ) ;
#11755=CARTESIAN_POINT ( 'NONE',  ( 3.799999999999999822, 0.000000000000000000, 50.00000000000000000 ) ) ;
#11775=ORIENTED_EDGE ( 'NONE', *, *, #961, .F. ) ;
#11812=EDGE_LOOP ( 'NONE', ( #4675, #28054, #2889, #24251 ) ) ;
#11821=CARTESIAN_POINT ( 'NONE',  ( 3.799999999999999822, 4.653657836759942730E-16, -40.40000000000000568 ) ) ;
#11854=ORIENTED_EDGE ( 'NONE', *, *, #33776, .T. ) ;
#11927=ORIENTED_EDGE ( 'NONE', *, *, #6617, .T. ) ;
#11960=DIRECTION ( 'NONE',  ( 0.000000000000000000, 0.000000000000000000, -1.000000000000000000 ) ) ;
#12054=UNCERTAINTY_MEASURE_WITH_UNIT (LENGTH_MEASURE( 1.000000000000000082E-05 ), #13181, 'distance_accuracy_value', 'NONE');
#12090=ORIENTED_EDGE ( 'NONE', *, *, #6617, .F. ) ;
#12208=CARTESIAN_POINT ( 'NONE',  ( 4.000000000000000000, 4.898587196589412829E-16, -39.50000000000000711 ) ) ;
#12218=EDGE_CURVE ( 'NONE', #7350, #33894, #1217, .T. ) ;
#12246=CARTESIAN_POINT ( 'NONE',  ( 0.000000000000000000, 0.000000000000000000, -33.50000000000000711 ) ) ;
#12267=ORIENTED_EDGE ( 'NONE', *, *, #12218, .F. ) ;
#12269=DIRECTION ( 'NONE',  ( -1.000000000000000000, 0.000000000000000000, 0.000000000000000000 ) ) ;
#12391=CARTESIAN_POINT ( 'NONE',  ( 0.000000000000000000, 0.000000000000000000, -39.50000000000000711 ) ) ;
#12415=EDGE_CURVE ( 'NONE', #27904, #33894, #114, .T. ) ;
#12451=COLOUR_RGB ( '', 0.40784314, 0.44705882, 0.49803922) ;
#12505=DIRECTION ( 'NONE',  ( 0.000000000000000000, 0.000000000000000000, 1.000000000000000000 ) ) ;
#12622=DIRECTION ( 'NONE',  ( 0.000000000000000000, 0.000000000000000000, 1.000000000000000000 ) ) ;
#12637=ORIENTED_EDGE ( 'NONE', *, *, #10768, .T. ) ;
#12725=DIRECTION ( 'NONE',  ( 0.000000000000000000, 0.000000000000000000, 1.000000000000000000 ) ) ;
#12847=CARTESIAN_POINT ( 'NONE',  ( 0.000000000000000000, 0.000000000000000000, 50.00000000000000000 ) ) ;
#12903=CYLINDRICAL_SURFACE ( 'NONE', #33943, 4.000000000000000000 ) ;
#12918=CIRCLE ( 'NONE', #34769, 4.000000000000000000 ) ;
#12949=ORIENTED_EDGE ( 'NONE', *, *, #1777, .T. ) ;
#12982=DIRECTION ( 'NONE',  ( 0.000000000000000000, 0.000000000000000000, -1.000000000000000000 ) ) ;
#13025=CIRCLE ( 'NONE', #33142, 4.000000000000000000 ) ;
#13061=CARTESIAN_POINT ( 'NONE',  ( -4.000000000000000000, 0.000000000000000000, 55.00000000000000000 ) ) ;
#13103=CARTESIAN_POINT ( 'NONE',  ( 0.000000000000000000, 0.000000000000000000, -33.50000000000000711 ) ) ;
#13110=LINE ( 'NONE', #4655, #1821 ) ;
#13173=ORIENTED_EDGE ( 'NONE', *, *, #35575, .F. ) ;
#13181=( LENGTH_UNIT ( ) NAMED_UNIT ( * ) SI_UNIT ( .MILLI., .METRE. ) );
#13182=DIRECTION ( 'NONE',  ( -1.000000000000000000, 0.000000000000000000, 0.000000000000000000 ) ) ;
#13221=AXIS2_PLACEMENT_3D ( 'NONE', #25417, #30467, #9194 ) ;
#13229=ADVANCED_FACE ( 'NONE', ( #32894 ), #8042, .F. ) ;
#13287=DIRECTION ( 'NONE',  ( 1.000000000000000000, 0.000000000000000000, 0.000000000000000000 ) ) ;
#13519=CARTESIAN_POINT ( 'NONE',  ( 3.799999999999999822, 4.653657836759942730E-16, -39.50000000000000711 ) ) ;
#13574=CARTESIAN_POINT ( 'NONE',  ( 0.000000000000000000, 0.000000000000000000, -34.40000000000000568 ) ) ;
#13629=PLANE ( 'NONE',  #22129 ) ;
#13667=DIRECTION ( 'NONE',  ( 0.000000000000000000, 0.000000000000000000, -1.000000000000000000 ) ) ;
#13705=VECTOR ( 'NONE', #14906, 1000.000000000000000 ) ;
#13721=CIRCLE ( 'NONE', #27528, 3.799999999999999822 ) ;
#13805=DIRECTION ( 'NONE',  ( 0.000000000000000000, 0.000000000000000000, 1.000000000000000000 ) ) ;
#13830=ORIENTED_EDGE ( 'NONE', *, *, #31329, .F. ) ;
#13848=ORIENTED_EDGE ( 'NONE', *, *, #20809, .F. ) ;
#13901=DIRECTION ( 'NONE',  ( 0.000000000000000000, 0.000000000000000000, -1.000000000000000000 ) ) ;
#13919=COLOUR_RGB ( '', 0.40784314, 0.44705882, 0.49803922) ;
#13933=ADVANCED_FACE ( 'NONE', ( #4838, #35433 ), #27516, .F. ) ;
#13953=ORIENTED_EDGE ( 'NONE', *, *, #3789, .T. ) ;
#13986=ORIENTED_EDGE ( 'NONE', *, *, #6825, .F. ) ;
#13994=CARTESIAN_POINT ( 'NONE',  ( 3.799999999999999822, 4.653657836759942730E-16, -33.50000000000000711 ) ) ;
#14051=( LENGTH_UNIT ( ) NAMED_UNIT ( * ) SI_UNIT ( .MILLI., .METRE. ) );
#14058=CARTESIAN_POINT ( 'NONE',  ( 0.000000000000000000, 0.000000000000000000, -40.40000000000000568 ) ) ;
#14126=EDGE_CURVE ( 'NONE', #11644, #485, #27687, .T. ) ;
#14154=ADVANCED_FACE ( 'NONE', ( #31083, #17377 ), #28378, .T. ) ;
#14197=AXIS2_PLACEMENT_3D ( 'NONE', #32534, #19033, #21911 ) ;
#14221=APPLICATION_CONTEXT ( 'automotive_design' ) ;
#14349=FACE_OUTER_BOUND ( 'NONE', #19283, .T. ) ;
#14372=CARTESIAN_POINT ( 'NONE',  ( -4.000000000000000000, 0.000000000000000000, -49.10000000000000142 ) ) ;
#14391=CIRCLE ( 'NONE', #2917, 4.000000000000000000 ) ;
#14403=SURFACE_SIDE_STYLE ('',( #28282 ) ) ;
#14644=AXIS2_PLACEMENT_3D ( 'NONE', #7868, #10941, #22083 ) ;
#14715=AXIS2_PLACEMENT_3D ( 'NONE', #29043, #31739, #1870 ) ;
#14730=EDGE_LOOP ( 'NONE', ( #34189, #33752 ) ) ;
#14761=ORIENTED_EDGE ( 'NONE', *, *, #11203, .F. ) ;
#14872=DIRECTION ( 'NONE',  ( -1.000000000000000000, 0.000000000000000000, 0.000000000000000000 ) ) ;
#14883=CARTESIAN_POINT ( 'NONE',  ( 4.000000000000000000, 4.898587196589412829E-16, -55.00000000000000000 ) ) ;
#14906=DIRECTION ( 'NONE',  ( 0.000000000000000000, 0.000000000000000000, -1.000000000000000000 ) ) ;
#14910=CIRCLE ( 'NONE', #29895, 4.000000000000000000 ) ;
#14926=DIRECTION ( 'NONE',  ( 0.000000000000000000, 0.000000000000000000, -1.000000000000000000 ) ) ;
#14928=CARTESIAN_POINT ( 'NONE',  ( 4.000000000000000000, 4.898587196589412829E-16, -49.10000000000000142 ) ) ;
#14939=VERTEX_POINT ( 'NONE', #7783 ) ;
#14953=CARTESIAN_POINT ( 'NONE',  ( 0.000000000000000000, 0.000000000000000000, -33.50000000000000711 ) ) ;
#14963=ORIENTED_EDGE ( 'NONE', *, *, #22015, .F. ) ;
#15067=FACE_BOUND ( 'NONE', #20270, .T. ) ;
#15204=CARTESIAN_POINT ( 'NONE',  ( 0.000000000000000000, 0.000000000000000000, -49.10000000000000142 ) ) ;
#15268=ORIENTED_EDGE ( 'NONE', *, *, #32356, .T. ) ;
#15347=DIRECTION ( 'NONE',  ( -1.000000000000000000, 0.000000000000000000, 0.000000000000000000 ) ) ;
#15518=DIRECTION ( 'NONE',  ( -1.000000000000000000, 0.000000000000000000, 0.000000000000000000 ) ) ;
#15537=CARTESIAN_POINT ( 'NONE',  ( 3.799999999999999822, 4.653657836759942730E-16, -39.50000000000000711 ) ) ;
#15690=DIRECTION ( 'NONE',  ( -1.000000000000000000, 0.000000000000000000, 0.000000000000000000 ) ) ;
#15699=DIRECTION ( 'NONE',  ( 1.000000000000000000, 0.000000000000000000, 0.000000000000000000 ) ) ;
#15736=ADVANCED_FACE ( 'NONE', ( #18510 ), #26275, .T. ) ;
#15825=DIRECTION ( 'NONE',  ( 0.000000000000000000, 0.000000000000000000, -1.000000000000000000 ) ) ;
#15842=DIRECTION ( 'NONE',  ( -1.000000000000000000, 0.000000000000000000, 0.000000000000000000 ) ) ;
#15862=CARTESIAN_POINT ( 'NONE',  ( -4.000000000000000000, 0.000000000000000000, 55.00000000000000000 ) ) ;
#15864=EDGE_CURVE ( 'NONE', #17076, #2951, #5631, .T. ) ;
#15866=VERTEX_POINT ( 'NONE', #13994 ) ;
#15871=EDGE_LOOP ( 'NONE', ( #32132, #22205, #34006, #7933 ) ) ;
#15878=STYLED_ITEM ( 'NONE', ( #32979 ), #22133 ) ;
#15981=VERTEX_POINT ( 'NONE', #21739 ) ;
#16001=CARTESIAN_POINT ( 'NONE',  ( 4.000000000000000000, 4.898587196589412829E-16, -50.00000000000000000 ) ) ;
#16046=APPLICATION_CONTEXT ( 'automotive_design' ) ;
#16088=ORIENTED_EDGE ( 'NONE', *, *, #31329, .T. ) ;
#16116=ORIENTED_EDGE ( 'NONE', *, *, #16747, .F. ) ;
#16144=EDGE_CURVE ( 'NONE', #33826, #27904, #7800, .T. ) ;
#16259=DIRECTION ( 'NONE',  ( 0.000000000000000000, 0.000000000000000000, -1.000000000000000000 ) ) ;
#16288=DIRECTION ( 'NONE',  ( -1.000000000000000000, 0.000000000000000000, 0.000000000000000000 ) ) ;
#16328=CARTESIAN_POINT ( 'NONE',  ( 0.000000000000000000, 0.000000000000000000, -33.50000000000000711 ) ) ;
#16360=ORIENTED_EDGE ( 'NONE', *, *, #26464, .F. ) ;
#16417=AXIS2_PLACEMENT_3D ( 'NONE', #19238, #5582, #33294 ) ;
#16491=CARTESIAN_POINT ( 'NONE',  ( 0.000000000000000000, 0.000000000000000000, -50.00000000000000000 ) ) ;
#16492=CIRCLE ( 'NONE', #11347, 4.000000000000000000 ) ;
#16505=DIRECTION ( 'NONE',  ( 0.000000000000000000, 0.000000000000000000, -1.000000000000000000 ) ) ;
#16559=DIRECTION ( 'NONE',  ( -1.000000000000000000, 0.000000000000000000, 0.000000000000000000 ) ) ;
#16566=SURFACE_SIDE_STYLE ('',( #32961 ) ) ;
#16603=VERTEX_POINT ( 'NONE', #15537 ) ;
#16630=DIRECTION ( 'NONE',  ( 0.000000000000000000, 0.000000000000000000, -1.000000000000000000 ) ) ;
#16686=DIRECTION ( 'NONE',  ( 0.000000000000000000, 0.000000000000000000, -1.000000000000000000 ) ) ;
#16717=ORIENTED_EDGE ( 'NONE', *, *, #35432, .T. ) ;
#16747=EDGE_CURVE ( 'NONE', #7350, #33826, #30403, .T. ) ;
#16781=VECTOR ( 'NONE', #6600, 1000.000000000000000 ) ;
#16782=( GEOMETRIC_REPRESENTATION_CONTEXT ( 3 ) GLOBAL_UNCERTAINTY_ASSIGNED_CONTEXT ( ( #20312 ) ) GLOBAL_UNIT_ASSIGNED_CONTEXT ( ( #8983, #8634, #2742 ) ) REPRESENTATION_CONTEXT ( 'NONE', 'WORKASPACE' ) );
#16951=EDGE_CURVE ( 'NONE', #8832, #19841, #1692, .T. ) ;
#16970=DIRECTION ( 'NONE',  ( 0.000000000000000000, 0.000000000000000000, -1.000000000000000000 ) ) ;
#17041=FACE_OUTER_BOUND ( 'NONE', #7667, .T. ) ;
#17076=VERTEX_POINT ( 'NONE', #8515 ) ;
#17102=CYLINDRICAL_SURFACE ( 'NONE', #25034, 4.000000000000000000 ) ;
#17104=EDGE_LOOP ( 'NONE', ( #9482, #17209 ) ) ;
#17141=CARTESIAN_POINT ( 'NONE',  ( 3.799999999999999822, 4.653657836759942730E-16, -33.50000000000000711 ) ) ;
#17166=EDGE_CURVE ( 'NONE', #25611, #16603, #21796, .T. ) ;
#17209=ORIENTED_EDGE ( 'NONE', *, *, #16951, .F. ) ;
#17257=ORIENTED_EDGE ( 'NONE', *, *, #17166, .F. ) ;
#17377=FACE_OUTER_BOUND ( 'NONE', #14730, .T. ) ;
#17403=DIRECTION ( 'NONE',  ( 0.000000000000000000, 0.000000000000000000, -1.000000000000000000 ) ) ;
#17414=DIRECTION ( 'NONE',  ( -1.000000000000000000, 0.000000000000000000, 0.000000000000000000 ) ) ;
#17470=CIRCLE ( 'NONE', #30720, 3.799999999999999822 ) ;
#17520=ORIENTED_EDGE ( 'NONE', *, *, #5964, .T. ) ;
#17576=ADVANCED_FACE ( 'NONE', ( #14349 ), #30410, .T. ) ;
#17633=FACE_OUTER_BOUND ( 'NONE', #35581, .T. ) ;
#17717=CARTESIAN_POINT ( 'NONE',  ( 0.000000000000000000, 0.000000000000000000, 49.10000000000000142 ) ) ;
#17737=DIRECTION ( 'NONE',  ( 0.000000000000000000, 0.000000000000000000, -1.000000000000000000 ) ) ;
#17756=VERTEX_POINT ( 'NONE', #14883 ) ;
#17951=PLANE ( 'NONE',  #4318 ) ;
#17953=DIRECTION ( 'NONE',  ( 0.000000000000000000, 0.000000000000000000, -1.000000000000000000 ) ) ;
#17967=CARTESIAN_POINT ( 'NONE',  ( 3.799999999999999822, 4.653657836759942730E-16, -34.40000000000000568 ) ) ;
#18070=DIRECTION ( 'NONE',  ( 1.000000000000000000, 0.000000000000000000, 0.000000000000000000 ) ) ;
#18117=EDGE_LOOP ( 'NONE', ( #27274, #35212 ) ) ;
#18142=PRODUCT ( 'shaft1', 'shaft1', '', ( #8759 ) ) ;
#18231=CARTESIAN_POINT ( 'NONE',  ( 0.000000000000000000, 0.000000000000000000, -39.50000000000000711 ) ) ;
#18292=DIRECTION ( 'NONE',  ( 1.000000000000000000, 0.000000000000000000, 0.000000000000000000 ) ) ;
#18328=DIRECTION ( 'NONE',  ( -1.000000000000000000, 0.000000000000000000, 0.000000000000000000 ) ) ;
#18384=ORIENTED_EDGE ( 'NONE', *, *, #4870, .F. ) ;
#18411=CARTESIAN_POINT ( 'NONE',  ( 0.000000000000000000, 0.000000000000000000, -55.00000000000000000 ) ) ;
#18433=DIRECTION ( 'NONE',  ( 0.000000000000000000, 0.000000000000000000, -1.000000000000000000 ) ) ;
#18494=FACE_OUTER_BOUND ( 'NONE', #5125, .T. ) ;
#18510=FACE_OUTER_BOUND ( 'NONE', #15871, .T. ) ;
#18512=STYLED_ITEM ( 'NONE', ( #30781 ), #39 ) ;
#18522=EDGE_CURVE ( 'NONE', #20307, #29572, #13721, .T. ) ;
#18648=CARTESIAN_POINT ( 'NONE',  ( 0.000000000000000000, 0.000000000000000000, -33.50000000000000711 ) ) ;
#18676=CYLINDRICAL_SURFACE ( 'NONE', #21672, 4.000000000000000000 ) ;
#18763=AXIS2_PLACEMENT_3D ( 'NONE', #9558, #28467, #3814 ) ;
#18779=ADVANCED_FACE ( 'NONE', ( #17633 ), #29352, .T. ) ;
#18847=DIRECTION ( 'NONE',  ( 0.000000000000000000, 0.000000000000000000, -1.000000000000000000 ) ) ;
#18850=AXIS2_PLACEMENT_3D ( 'NONE', #7700, #10055, #21022 ) ;
#18936=CARTESIAN_POINT ( 'NONE',  ( 0.000000000000000000, 0.000000000000000000, 50.00000000000000000 ) ) ;
#18948=AXIS2_PLACEMENT_3D ( 'NONE', #8423, #13667, #5737 ) ;
#19026=DIRECTION ( 'NONE',  ( 0.000000000000000000, 0.000000000000000000, -1.000000000000000000 ) ) ;
#19033=DIRECTION ( 'NONE',  ( 0.000000000000000000, 0.000000000000000000, -1.000000000000000000 ) ) ;
#19130=EDGE_LOOP ( 'NONE', ( #30566, #24152, #26142, #12267 ) ) ;
#19141=DIRECTION ( 'NONE',  ( -1.000000000000000000, 0.000000000000000000, 0.000000000000000000 ) ) ;
#19178=DIRECTION ( 'NONE',  ( 0.000000000000000000, 0.000000000000000000, -1.000000000000000000 ) ) ;
#19193=ADVANCED_FACE ( 'NONE', ( #10732, #5690 ), #32701, .T. ) ;
#19213=CARTESIAN_POINT ( 'NONE',  ( 0.000000000000000000, 0.000000000000000000, -49.10000000000000142 ) ) ;
#19238=CARTESIAN_POINT ( 'NONE',  ( 0.000000000000000000, 0.000000000000000000, 55.00000000000000000 ) ) ;
#19254=EDGE_LOOP ( 'NONE', ( #32644, #21249, #23284, #23598 ) ) ;
#19283=EDGE_LOOP ( 'NONE', ( #25918, #24707, #845, #5719 ) ) ;
#19330=LINE ( 'NONE', #5671, #7293 ) ;
#19449=ORIENTED_EDGE ( 'NONE', *, *, #23108, .F. ) ;
#19469=CARTESIAN_POINT ( 'NONE',  ( 0.000000000000000000, 0.000000000000000000, -39.50000000000000711 ) ) ;
#19535=CYLINDRICAL_SURFACE ( 'NONE', #7331, 4.000000000000000000 ) ;
#19561=LINE ( 'NONE', #316, #32843 ) ;
#19594=DIRECTION ( 'NONE',  ( -1.000000000000000000, 0.000000000000000000, 0.000000000000000000 ) ) ;
#19647=ORIENTED_EDGE ( 'NONE', *, *, #6555, .F. ) ;
#19683=EDGE_LOOP ( 'NONE', ( #14761, #21913 ) ) ;
#19712=CARTESIAN_POINT ( 'NONE',  ( -4.000000000000000000, 0.000000000000000000, 49.10000000000000142 ) ) ;
#19724=ORIENTED_EDGE ( 'NONE', *, *, #21736, .F. ) ;
#19738=AXIS2_PLACEMENT_3D ( 'NONE', #29373, #12982, #32948 ) ;
#19794=DIRECTION ( 'NONE',  ( -1.000000000000000000, 0.000000000000000000, 0.000000000000000000 ) ) ;
#19841=VERTEX_POINT ( 'NONE', #3702 ) ;
#19870=VECTOR ( 'NONE', #2398, 1000.000000000000000 ) ;
#19890=CARTESIAN_POINT ( 'NONE',  ( 3.799999999999999822, 0.000000000000000000, 49.10000000000000142 ) ) ;
#19947=ORIENTED_EDGE ( 'NONE', *, *, #5784, .T. ) ;
#19977=CARTESIAN_POINT ( 'NONE',  ( -4.000000000000000000, 0.000000000000000000, -50.00000000000000000 ) ) ;
#20068=FACE_OUTER_BOUND ( 'NONE', #19130, .T. ) ;
#20140=AXIS2_PLACEMENT_3D ( 'NONE', #31887, #27217, #13182 ) ;
#20173=EDGE_CURVE ( 'NONE', #31617, #15981, #35111, .T. ) ;
#20180=VERTEX_POINT ( 'NONE', #2608 ) ;
#20200=DIRECTION ( 'NONE',  ( 0.000000000000000000, 0.000000000000000000, -1.000000000000000000 ) ) ;
#20201=CARTESIAN_POINT ( 'NONE',  ( 4.000000000000000000, 4.898587196589412829E-16, 50.00000000000000000 ) ) ;
#20232=ORIENTED_EDGE ( 'NONE', *, *, #30791, .F. ) ;
#20252=ORIENTED_EDGE ( 'NONE', *, *, #304, .F. ) ;
#20270=EDGE_LOOP ( 'NONE', ( #12949, #30260 ) ) ;
#20298=CARTESIAN_POINT ( 'NONE',  ( 0.000000000000000000, 0.000000000000000000, -39.50000000000000711 ) ) ;
#20307=VERTEX_POINT ( 'NONE', #589 ) ;
#20308=VERTEX_POINT ( 'NONE', #5658 ) ;
#20312=UNCERTAINTY_MEASURE_WITH_UNIT (LENGTH_MEASURE( 1.000000000000000082E-05 ), #8983, 'distance_accuracy_value', 'NONE');
#20475=CARTESIAN_POINT ( 'NONE',  ( -4.000000000000000000, 0.000000000000000000, -33.50000000000000711 ) ) ;
#20541=AXIS2_PLACEMENT_3D ( 'NONE', #15204, #20786, #26039 ) ;
#20623=EDGE_CURVE ( 'NONE', #26766, #3989, #10960, .T. ) ;
#20786=DIRECTION ( 'NONE',  ( 0.000000000000000000, 0.000000000000000000, -1.000000000000000000 ) ) ;
#20809=EDGE_CURVE ( 'NONE', #27386, #10958, #13110, .T. ) ;
#20847=ORIENTED_EDGE ( 'NONE', *, *, #961, .T. ) ;
#20852=AXIS2_PLACEMENT_3D ( 'NONE', #2354, #10444, #23764 ) ;
#20974=DIRECTION ( 'NONE',  ( 0.000000000000000000, 0.000000000000000000, -1.000000000000000000 ) ) ;
#21022=DIRECTION ( 'NONE',  ( 1.000000000000000000, 0.000000000000000000, 0.000000000000000000 ) ) ;
#21163=ADVANCED_FACE ( 'NONE', ( #25671 ), #8908, .T. ) ;
#21246=ORIENTED_EDGE ( 'NONE', *, *, #29229, .F. ) ;
#21249=ORIENTED_EDGE ( 'NONE', *, *, #26520, .T. ) ;
#21257=CARTESIAN_POINT ( 'NONE',  ( 0.000000000000000000, 0.000000000000000000, -34.40000000000000568 ) ) ;
#21276=AXIS2_PLACEMENT_3D ( 'NONE', #5308, #18433, #19141 ) ;
#21278=DIRECTION ( 'NONE',  ( 0.000000000000000000, 0.000000000000000000, -1.000000000000000000 ) ) ;
#21307=AXIS2_PLACEMENT_3D ( 'NONE', #26589, #12725, #18292 ) ;
#21431=FACE_BOUND ( 'NONE', #23472, .T. ) ;
#21467=ORIENTED_EDGE ( 'NONE', *, *, #20809, .T. ) ;
#21549=CIRCLE ( 'NONE', #23280, 3.799999999999999822 ) ;
#21629=CARTESIAN_POINT ( 'NONE',  ( 0.000000000000000000, 0.000000000000000000, 55.00000000000000000 ) ) ;
#21644=ORIENTED_EDGE ( 'NONE', *, *, #1787, .T. ) ;
#21653=ORIENTED_EDGE ( 'NONE', *, *, #5784, .F. ) ;
#21672=AXIS2_PLACEMENT_3D ( 'NONE', #29673, #16505, #27519 ) ;
#21703=DIRECTION ( 'NONE',  ( -1.000000000000000000, 0.000000000000000000, 0.000000000000000000 ) ) ;
#21736=EDGE_CURVE ( 'NONE', #24945, #17756, #5662, .T. ) ;
#21739=CARTESIAN_POINT ( 'NONE',  ( -3.799999999999999822, 0.000000000000000000, -40.40000000000000568 ) ) ;
#21773=AXIS2_PLACEMENT_3D ( 'NONE', #17717, #34115, #28715 ) ;
#21796=CIRCLE ( 'NONE', #34466, 3.799999999999999822 ) ;
#21799=CARTESIAN_POINT ( 'NONE',  ( -3.799999999999999822, 0.000000000000000000, -50.00000000000000000 ) ) ;
#21803=DIRECTION ( 'NONE',  ( 0.000000000000000000, 0.000000000000000000, -1.000000000000000000 ) ) ;
#21878=EDGE_LOOP ( 'NONE', ( #7770, #34684 ) ) ;
#21884=AXIS2_PLACEMENT_3D ( 'NONE', #18231, #34271, #15518 ) ;
#21911=DIRECTION ( 'NONE',  ( -1.000000000000000000, 0.000000000000000000, 0.000000000000000000 ) ) ;
#21913=ORIENTED_EDGE ( 'NONE', *, *, #32356, .F. ) ;
#21962=FILL_AREA_STYLE ('',( #33650 ) ) ;
#21975=CARTESIAN_POINT ( 'NONE',  ( 0.000000000000000000, 0.000000000000000000, -34.40000000000000568 ) ) ;
#21979=CIRCLE ( 'NONE', #32347, 4.000000000000000000 ) ;
#22015=EDGE_CURVE ( 'NONE', #20308, #14939, #32802, .T. ) ;
#22040=CARTESIAN_POINT ( 'NONE',  ( -3.799999999999999822, 0.000000000000000000, -49.10000000000000142 ) ) ;
#22078=DIRECTION ( 'NONE',  ( 0.000000000000000000, 0.000000000000000000, -1.000000000000000000 ) ) ;
#22083=DIRECTION ( 'NONE',  ( -1.000000000000000000, 0.000000000000000000, 0.000000000000000000 ) ) ;
#22129=AXIS2_PLACEMENT_3D ( 'NONE', #120, #22078, #292 ) ;
#22133=MANIFOLD_SOLID_BREP ( 'LPattern2', #34219 ) ;
#22141=SURFACE_STYLE_USAGE ( .BOTH. , #16566 ) ;
#22158=SURFACE_STYLE_USAGE ( .BOTH. , #14403 ) ;
#22205=ORIENTED_EDGE ( 'NONE', *, *, #1777, .F. ) ;
#22209=ADVANCED_FACE ( 'NONE', ( #8485 ), #5792, .T. ) ;
#22312=VECTOR ( 'NONE', #35363, 1000.000000000000000 ) ;
#22319=SHAPE_REPRESENTATION_RELATIONSHIP ( 'NONE' , 'NONE' ,  #33742, #39 ) ;
#22372=DIRECTION ( 'NONE',  ( 0.000000000000000000, 0.000000000000000000, -1.000000000000000000 ) ) ;
#22618=EDGE_LOOP ( 'NONE', ( #16116, #19647 ) ) ;
#22663=EDGE_LOOP ( 'NONE', ( #13953, #9045, #7728, #58 ) ) ;
#22676=( NAMED_UNIT ( * ) PLANE_ANGLE_UNIT ( ) SI_UNIT ( $, .RADIAN. ) );
#22873=DIRECTION ( 'NONE',  ( 0.000000000000000000, 0.000000000000000000, -1.000000000000000000 ) ) ;
#22899=DIRECTION ( 'NONE',  ( -1.000000000000000000, 0.000000000000000000, 0.000000000000000000 ) ) ;
#22991=CARTESIAN_POINT ( 'NONE',  ( 0.000000000000000000, 0.000000000000000000, -49.10000000000000142 ) ) ;
#23002=DIRECTION ( 'NONE',  ( 0.000000000000000000, 0.000000000000000000, -1.000000000000000000 ) ) ;
#23031=AXIS2_PLACEMENT_3D ( 'NONE', #34690, #9662, #14872 ) ;
#23043=FACE_OUTER_BOUND ( 'NONE', #9674, .T. ) ;
#23108=EDGE_CURVE ( 'NONE', #10958, #14939, #11652, .T. ) ;
#23157=LINE ( 'NONE', #23516, #18 ) ;
#23193=DIRECTION ( 'NONE',  ( 0.000000000000000000, 0.000000000000000000, -1.000000000000000000 ) ) ;
#23219=DIRECTION ( 'NONE',  ( -1.000000000000000000, 0.000000000000000000, 0.000000000000000000 ) ) ;
#23272=FACE_BOUND ( 'NONE', #26132, .T. ) ;
#23280=AXIS2_PLACEMENT_3D ( 'NONE', #16491, #32896, #24795 ) ;
#23284=ORIENTED_EDGE ( 'NONE', *, *, #9986, .T. ) ;
#23333=DIRECTION ( 'NONE',  ( 0.000000000000000000, 0.000000000000000000, -1.000000000000000000 ) ) ;
#23366=ORIENTED_EDGE ( 'NONE', *, *, #522, .T. ) ;
#23472=EDGE_LOOP ( 'NONE', ( #34193, #34645 ) ) ;
#23516=CARTESIAN_POINT ( 'NONE',  ( 4.000000000000000000, 4.898587196589412829E-16, 55.00000000000000000 ) ) ;
#23584=VECTOR ( 'NONE', #11513, 1000.000000000000000 ) ;
#23589=ORIENTED_EDGE ( 'NONE', *, *, #31485, .T. ) ;
#23591=DIRECTION ( 'NONE',  ( 0.000000000000000000, 0.000000000000000000, 1.000000000000000000 ) ) ;
#23598=ORIENTED_EDGE ( 'NONE', *, *, #14126, .F. ) ;
#23650=CYLINDRICAL_SURFACE ( 'NONE', #21884, 3.799999999999999822 ) ;
#23738=DIRECTION ( 'NONE',  ( 0.000000000000000000, 0.000000000000000000, -1.000000000000000000 ) ) ;
#23746=LINE ( 'NONE', #24290, #25392 ) ;
#23751=AXIS2_PLACEMENT_3D ( 'NONE', #5868, #1004, #3180 ) ;
#23764=DIRECTION ( 'NONE',  ( -1.000000000000000000, 0.000000000000000000, 0.000000000000000000 ) ) ;
#23825=CARTESIAN_POINT ( 'NONE',  ( 0.000000000000000000, 0.000000000000000000, -33.50000000000000711 ) ) ;
#24075=VERTEX_POINT ( 'NONE', #26785 ) ;
#24123=ORIENTED_EDGE ( 'NONE', *, *, #4870, .T. ) ;
#24152=ORIENTED_EDGE ( 'NONE', *, *, #16144, .T. ) ;
#24183=FACE_OUTER_BOUND ( 'NONE', #25029, .T. ) ;
#24246=ORIENTED_EDGE ( 'NONE', *, *, #16951, .T. ) ;
#24251=ORIENTED_EDGE ( 'NONE', *, *, #522, .F. ) ;
#24290=CARTESIAN_POINT ( 'NONE',  ( -3.799999999999999822, 0.000000000000000000, -33.50000000000000711 ) ) ;
#24486=ORIENTED_EDGE ( 'NONE', *, *, #26796, .F. ) ;
#24507=FACE_OUTER_BOUND ( 'NONE', #7753, .T. ) ;
#24539=DIRECTION ( 'NONE',  ( -1.000000000000000000, 0.000000000000000000, 0.000000000000000000 ) ) ;
#24596=VERTEX_POINT ( 'NONE', #30464 ) ;
#24637=FACE_BOUND ( 'NONE', #34889, .T. ) ;
#24677=CYLINDRICAL_SURFACE ( 'NONE', #29944, 4.000000000000000000 ) ;
#24707=ORIENTED_EDGE ( 'NONE', *, *, #6555, .T. ) ;
#24741=DIRECTION ( 'NONE',  ( 0.000000000000000000, 0.000000000000000000, -1.000000000000000000 ) ) ;
#24780=AXIS2_PLACEMENT_3D ( 'NONE', #21257, #10471, #15842 ) ;
#24795=DIRECTION ( 'NONE',  ( -1.000000000000000000, 0.000000000000000000, 0.000000000000000000 ) ) ;
#24808=FACE_OUTER_BOUND ( 'NONE', #22663, .T. ) ;
#24815=DIRECTION ( 'NONE',  ( 0.000000000000000000, 0.000000000000000000, -1.000000000000000000 ) ) ;
#24855=ADVANCED_FACE ( 'NONE', ( #23043 ), #17102, .T. ) ;
#24896=CIRCLE ( 'NONE', #20852, 4.000000000000000000 ) ;
#24945=VERTEX_POINT ( 'NONE', #16001 ) ;
#24978=ORIENTED_EDGE ( 'NONE', *, *, #15864, .T. ) ;
#25029=EDGE_LOOP ( 'NONE', ( #28375, #24978, #31625, #21653 ) ) ;
#25034=AXIS2_PLACEMENT_3D ( 'NONE', #9189, #31335, #9367 ) ;
#25057=DIRECTION ( 'NONE',  ( 1.000000000000000000, 0.000000000000000000, 0.000000000000000000 ) ) ;
#25392=VECTOR ( 'NONE', #26814, 1000.000000000000000 ) ;
#25417=CARTESIAN_POINT ( 'NONE',  ( 0.000000000000000000, 0.000000000000000000, 50.00000000000000000 ) ) ;
#25556=ORIENTED_EDGE ( 'NONE', *, *, #30791, .T. ) ;
#25598=EDGE_LOOP ( 'NONE', ( #18384, #21467, #16360, #14963 ) ) ;
#25611=VERTEX_POINT ( 'NONE', #32895 ) ;
#25645=VECTOR ( 'NONE', #22372, 1000.000000000000000 ) ;
#25671=FACE_OUTER_BOUND ( 'NONE', #19254, .T. ) ;
#25685=CYLINDRICAL_SURFACE ( 'NONE', #8614, 4.000000000000000000 ) ;
#25705=AXIS2_PLACEMENT_3D ( 'NONE', #14953, #33692, #12269 ) ;
#25755=AXIS2_PLACEMENT_3D ( 'NONE', #19213, #16686, #30736 ) ;
#25803=AXIS2_PLACEMENT_3D ( 'NONE', #18648, #19178, #21703 ) ;
#25878=EDGE_LOOP ( 'NONE', ( #26036, #8473 ) ) ;
#25918=ORIENTED_EDGE ( 'NONE', *, *, #16144, .F. ) ;
#25994=FACE_OUTER_BOUND ( 'NONE', #35326, .T. ) ;
#26035=CARTESIAN_POINT ( 'NONE',  ( 0.000000000000000000, 0.000000000000000000, 55.00000000000000000 ) ) ;
#26036=ORIENTED_EDGE ( 'NONE', *, *, #35166, .T. ) ;
#26039=DIRECTION ( 'NONE',  ( -1.000000000000000000, 0.000000000000000000, 0.000000000000000000 ) ) ;
#26092=ORIENTED_EDGE ( 'NONE', *, *, #20173, .F. ) ;
#26132=EDGE_LOOP ( 'NONE', ( #26985, #6296 ) ) ;
#26142=ORIENTED_EDGE ( 'NONE', *, *, #35166, .F. ) ;
#26204=DIRECTION ( 'NONE',  ( -1.000000000000000000, 0.000000000000000000, 0.000000000000000000 ) ) ;
#26216=ORIENTED_EDGE ( 'NONE', *, *, #20173, .T. ) ;
#26243=EDGE_CURVE ( 'NONE', #2951, #3338, #11071, .T. ) ;
#26246=EDGE_CURVE ( 'NONE', #8832, #3989, #19330, .T. ) ;
#26275=CYLINDRICAL_SURFACE ( 'NONE', #18850, 3.799999999999999822 ) ;
#26464=EDGE_CURVE ( 'NONE', #14939, #10958, #9945, .T. ) ;
#26520=EDGE_CURVE ( 'NONE', #9824, #27576, #26669, .T. ) ;
#26589=CARTESIAN_POINT ( 'NONE',  ( 0.000000000000000000, 0.000000000000000000, 0.000000000000000000 ) ) ;
#26662=ORIENTED_EDGE ( 'NONE', *, *, #27146, .F. ) ;
#26669=LINE ( 'NONE', #1644, #10638 ) ;
#26766=VERTEX_POINT ( 'NONE', #14372 ) ;
#26785=CARTESIAN_POINT ( 'NONE',  ( -4.000000000000000000, 0.000000000000000000, -34.40000000000000568 ) ) ;
#26796=EDGE_CURVE ( 'NONE', #8680, #10339, #34774, .T. ) ;
#26814=DIRECTION ( 'NONE',  ( 0.000000000000000000, 0.000000000000000000, -1.000000000000000000 ) ) ;
#26891=DIRECTION ( 'NONE',  ( 0.000000000000000000, 0.000000000000000000, -1.000000000000000000 ) ) ;
#26985=ORIENTED_EDGE ( 'NONE', *, *, #34608, .F. ) ;
#27093=CIRCLE ( 'NONE', #10971, 4.000000000000000000 ) ;
#27146=EDGE_CURVE ( 'NONE', #29572, #20307, #30192, .T. ) ;
#27217=DIRECTION ( 'NONE',  ( 0.000000000000000000, 0.000000000000000000, -1.000000000000000000 ) ) ;
#27274=ORIENTED_EDGE ( 'NONE', *, *, #26464, .T. ) ;
#27277=DIRECTION ( 'NONE',  ( -1.000000000000000000, 0.000000000000000000, 0.000000000000000000 ) ) ;
#27386=VERTEX_POINT ( 'NONE', #8741 ) ;
#27424=CARTESIAN_POINT ( 'NONE',  ( 0.000000000000000000, 0.000000000000000000, -49.10000000000000142 ) ) ;
#27502=AXIS2_PLACEMENT_3D ( 'NONE', #12246, #14926, #23219 ) ;
#27516=PLANE ( 'NONE',  #14197 ) ;
#27519=DIRECTION ( 'NONE',  ( -1.000000000000000000, 0.000000000000000000, 0.000000000000000000 ) ) ;
#27528=AXIS2_PLACEMENT_3D ( 'NONE', #21975, #2922, #10307 ) ;
#27551=FACE_OUTER_BOUND ( 'NONE', #4400, .T. ) ;
#27576=VERTEX_POINT ( 'NONE', #30161 ) ;
#27687=LINE ( 'NONE', #19890, #1508 ) ;
#27758=CARTESIAN_POINT ( 'NONE',  ( 0.000000000000000000, 0.000000000000000000, 55.00000000000000000 ) ) ;
#27811=CARTESIAN_POINT ( 'NONE',  ( -4.000000000000000000, 0.000000000000000000, 55.00000000000000000 ) ) ;
#27812=ORIENTED_EDGE ( 'NONE', *, *, #15864, .F. ) ;
#27904=VERTEX_POINT ( 'NONE', #9607 ) ;
#27947=ORIENTED_EDGE ( 'NONE', *, *, #17166, .T. ) ;
#27960=AXIS2_PLACEMENT_3D ( 'NONE', #31576, #11960, #15347 ) ;
#27961=CARTESIAN_POINT ( 'NONE',  ( 0.000000000000000000, 0.000000000000000000, -40.40000000000000568 ) ) ;
#28042=ADVANCED_FACE ( 'NONE', ( #27551 ), #5754, .T. ) ;
#28054=ORIENTED_EDGE ( 'NONE', *, *, #35575, .T. ) ;
#28096=ORIENTED_EDGE ( 'NONE', *, *, #6825, .T. ) ;
#28272=ORIENTED_EDGE ( 'NONE', *, *, #7710, .F. ) ;
#28282=SURFACE_STYLE_FILL_AREA ( #5959 ) ;
#28375=ORIENTED_EDGE ( 'NONE', *, *, #33776, .F. ) ;
#28378=PLANE ( 'NONE',  #20541 ) ;
#28467=DIRECTION ( 'NONE',  ( 0.000000000000000000, 0.000000000000000000, -1.000000000000000000 ) ) ;
#28520=CARTESIAN_POINT ( 'NONE',  ( 3.799999999999999822, 4.653657836759942730E-16, -50.00000000000000000 ) ) ;
#28573=LINE ( 'NONE', #13519, #23584 ) ;
#28715=DIRECTION ( 'NONE',  ( -1.000000000000000000, 0.000000000000000000, 0.000000000000000000 ) ) ;
#28727=ORIENTED_EDGE ( 'NONE', *, *, #30275, .F. ) ;
#28773=AXIS2_PLACEMENT_3D ( 'NONE', #8215, #13805, #13287 ) ;
#28787=CARTESIAN_POINT ( 'NONE',  ( 4.000000000000000000, 4.898587196589412829E-16, 49.10000000000000142 ) ) ;
#29043=CARTESIAN_POINT ( 'NONE',  ( 0.000000000000000000, 0.000000000000000000, 49.10000000000000142 ) ) ;
#29053=AXIS2_PLACEMENT_3D ( 'NONE', #9644, #6400, #26204 ) ;
#29108=DIRECTION ( 'NONE',  ( -1.000000000000000000, 0.000000000000000000, 0.000000000000000000 ) ) ;
#29120=CARTESIAN_POINT ( 'NONE',  ( -4.000000000000000000, 0.000000000000000000, 55.00000000000000000 ) ) ;
#29205=AXIS2_PLACEMENT_3D ( 'NONE', #9247, #20200, #31208 ) ;
#29229=EDGE_CURVE ( 'NONE', #3338, #34725, #7896, .T. ) ;
#29352=CYLINDRICAL_SURFACE ( 'NONE', #27502, 3.799999999999999822 ) ;
#29373=CARTESIAN_POINT ( 'NONE',  ( 0.000000000000000000, 0.000000000000000000, -50.00000000000000000 ) ) ;
#29491=AXIS2_PLACEMENT_3D ( 'NONE', #18936, #21278, #15690 ) ;
#29503=CIRCLE ( 'NONE', #32369, 3.799999999999999822 ) ;
#29572=VERTEX_POINT ( 'NONE', #17967 ) ;
#29649=ORIENTED_EDGE ( 'NONE', *, *, #304, .T. ) ;
#29673=CARTESIAN_POINT ( 'NONE',  ( 0.000000000000000000, 0.000000000000000000, 55.00000000000000000 ) ) ;
#29704=AXIS2_PLACEMENT_3D ( 'NONE', #27758, #373, #3098 ) ;
#29767=DIRECTION ( 'NONE',  ( -1.000000000000000000, 0.000000000000000000, 0.000000000000000000 ) ) ;
#29895=AXIS2_PLACEMENT_3D ( 'NONE', #19469, #17953, #33161 ) ;
#29899=CARTESIAN_POINT ( 'NONE',  ( 0.000000000000000000, 0.000000000000000000, 50.00000000000000000 ) ) ;
#29944=AXIS2_PLACEMENT_3D ( 'NONE', #11346, #10991, #16559 ) ;
#29972=ADVANCED_FACE ( 'NONE', ( #24637, #11472 ), #30395, .T. ) ;
#29987=DIRECTION ( 'NONE',  ( -1.000000000000000000, 0.000000000000000000, 0.000000000000000000 ) ) ;
#30025=DIRECTION ( 'NONE',  ( -1.000000000000000000, 0.000000000000000000, 0.000000000000000000 ) ) ;
#30115=CYLINDRICAL_SURFACE ( 'NONE', #32252, 3.799999999999999822 ) ;
#30132=CARTESIAN_POINT ( 'NONE',  ( 4.000000000000000000, 4.898587196589412829E-16, 55.00000000000000000 ) ) ;
#30161=CARTESIAN_POINT ( 'NONE',  ( -3.799999999999999822, 4.653657836759942730E-16, 50.00000000000000000 ) ) ;
#30192=CIRCLE ( 'NONE', #14644, 3.799999999999999822 ) ;
#30211=VERTEX_POINT ( 'NONE', #6591 ) ;
#30260=ORIENTED_EDGE ( 'NONE', *, *, #31984, .T. ) ;
#30262=( NAMED_UNIT ( * ) PLANE_ANGLE_UNIT ( ) SI_UNIT ( $, .RADIAN. ) );
#30275=EDGE_CURVE ( 'NONE', #3989, #26766, #3750, .T. ) ;
#30284=FILL_AREA_STYLE_COLOUR ( '', #12451 ) ;
#30360=AXIS2_PLACEMENT_3D ( 'NONE', #4501, #6812, #18328 ) ;
#30373=DIRECTION ( 'NONE',  ( -1.000000000000000000, 0.000000000000000000, 0.000000000000000000 ) ) ;
#30380=FACE_OUTER_BOUND ( 'NONE', #21878, .T. ) ;
#30395=PLANE ( 'NONE',  #8260 ) ;
#30400=DIRECTION ( 'NONE',  ( 0.000000000000000000, 0.000000000000000000, -1.000000000000000000 ) ) ;
#30403=CIRCLE ( 'NONE', #21773, 4.000000000000000000 ) ;
#30410=CYLINDRICAL_SURFACE ( 'NONE', #18948, 4.000000000000000000 ) ;
#30435=ORIENTED_EDGE ( 'NONE', *, *, #31485, .F. ) ;
#30464=CARTESIAN_POINT ( 'NONE',  ( -4.000000000000000000, 0.000000000000000000, -55.00000000000000000 ) ) ;
#30467=DIRECTION ( 'NONE',  ( 0.000000000000000000, 0.000000000000000000, -1.000000000000000000 ) ) ;
#30566=ORIENTED_EDGE ( 'NONE', *, *, #16747, .T. ) ;
#30662=DIRECTION ( 'NONE',  ( 0.000000000000000000, 0.000000000000000000, -1.000000000000000000 ) ) ;
#30720=AXIS2_PLACEMENT_3D ( 'NONE', #20298, #23738, #31655 ) ;
#30736=DIRECTION ( 'NONE',  ( -1.000000000000000000, 0.000000000000000000, 0.000000000000000000 ) ) ;
#30774=AXIS2_PLACEMENT_3D ( 'NONE', #32828, #2421, #10507 ) ;
#30781=PRESENTATION_STYLE_ASSIGNMENT (( #22141 ) ) ;
#30791=EDGE_CURVE ( 'NONE', #2951, #17076, #32254, .T. ) ;
#30803=ADVANCED_FACE ( 'NONE', ( #21431, #24507 ), #10297, .F. ) ;
#30904=DIRECTION ( 'NONE',  ( 0.000000000000000000, 0.000000000000000000, 1.000000000000000000 ) ) ;
#31065=PRODUCT_DEFINITION_SHAPE ( 'NONE', 'NONE',  #3129 ) ;
#31079=AXIS2_PLACEMENT_3D ( 'NONE', #22991, #17403, #1224 ) ;
#31083=FACE_BOUND ( 'NONE', #31712, .T. ) ;
#31123=ORIENTED_EDGE ( 'NONE', *, *, #26243, .F. ) ;
#31157=DIRECTION ( 'NONE',  ( 1.000000000000000000, 0.000000000000000000, 0.000000000000000000 ) ) ;
#31162=MECHANICAL_DESIGN_GEOMETRIC_PRESENTATION_REPRESENTATION('',(#18512),#16782);
#31208=DIRECTION ( 'NONE',  ( -1.000000000000000000, 0.000000000000000000, 0.000000000000000000 ) ) ;
#31232=CIRCLE ( 'NONE', #11693, 3.799999999999999822 ) ;
#31329=EDGE_CURVE ( 'NONE', #20180, #20307, #23746, .T. ) ;
#31335=DIRECTION ( 'NONE',  ( 0.000000000000000000, 0.000000000000000000, -1.000000000000000000 ) ) ;
#31485=EDGE_CURVE ( 'NONE', #10090, #24596, #19561, .T. ) ;
#31498=ADVANCED_FACE ( 'NONE', ( #17041 ), #499, .T. ) ;
#31554=DIRECTION ( 'NONE',  ( 0.000000000000000000, 0.000000000000000000, -1.000000000000000000 ) ) ;
#31576=CARTESIAN_POINT ( 'NONE',  ( 0.000000000000000000, 0.000000000000000000, 50.00000000000000000 ) ) ;
#31617=VERTEX_POINT ( 'NONE', #11821 ) ;
#31625=ORIENTED_EDGE ( 'NONE', *, *, #26243, .T. ) ;
#31655=DIRECTION ( 'NONE',  ( -1.000000000000000000, 0.000000000000000000, 0.000000000000000000 ) ) ;
#31712=EDGE_LOOP ( 'NONE', ( #20232, #27812 ) ) ;
#31739=DIRECTION ( 'NONE',  ( 0.000000000000000000, 0.000000000000000000, -1.000000000000000000 ) ) ;
#31741=DIRECTION ( 'NONE',  ( 0.000000000000000000, 0.000000000000000000, -1.000000000000000000 ) ) ;
#31768=VECTOR ( 'NONE', #16970, 1000.000000000000000 ) ;
#31791=AXIS2_PLACEMENT_3D ( 'NONE', #29899, #15825, #34959 ) ;
#31887=CARTESIAN_POINT ( 'NONE',  ( 0.000000000000000000, 0.000000000000000000, -49.10000000000000142 ) ) ;
#31922=AXIS2_PLACEMENT_3D ( 'NONE', #7513, #19026, #30025 ) ;
#31977=FACE_OUTER_BOUND ( 'NONE', #2287, .T. ) ;
#31984=EDGE_CURVE ( 'NONE', #9824, #11644, #8180, .T. ) ;
#32132=ORIENTED_EDGE ( 'NONE', *, *, #26520, .F. ) ;
#32160=FACE_OUTER_BOUND ( 'NONE', #1999, .T. ) ;
#32252=AXIS2_PLACEMENT_3D ( 'NONE', #27424, #13901, #24539 ) ;
#32254=CIRCLE ( 'NONE', #20140, 3.799999999999999822 ) ;
#32347=AXIS2_PLACEMENT_3D ( 'NONE', #1894, #12505, #18070 ) ;
#32356=EDGE_CURVE ( 'NONE', #17756, #24596, #21979, .T. ) ;
#32369=AXIS2_PLACEMENT_3D ( 'NONE', #81, #16259, #27277 ) ;
#32514=DIRECTION ( 'NONE',  ( -1.000000000000000000, 0.000000000000000000, 0.000000000000000000 ) ) ;
#32534=CARTESIAN_POINT ( 'NONE',  ( 0.000000000000000000, 0.000000000000000000, -40.40000000000000568 ) ) ;
#32551=CIRCLE ( 'NONE', #27960, 3.799999999999999822 ) ;
#32635=DIRECTION ( 'NONE',  ( 0.000000000000000000, 0.000000000000000000, 1.000000000000000000 ) ) ;
#32644=ORIENTED_EDGE ( 'NONE', *, *, #31984, .F. ) ;
#32699=ORIENTED_EDGE ( 'NONE', *, *, #21736, .T. ) ;
#32701=PLANE ( 'NONE',  #25803 ) ;
#32802=LINE ( 'NONE', #15862, #19870 ) ;
#32828=CARTESIAN_POINT ( 'NONE',  ( 0.000000000000000000, 0.000000000000000000, -49.10000000000000142 ) ) ;
#32843=VECTOR ( 'NONE', #30400, 1000.000000000000000 ) ;
#32890=( GEOMETRIC_REPRESENTATION_CONTEXT ( 3 ) GLOBAL_UNCERTAINTY_ASSIGNED_CONTEXT ( ( #12054 ) ) GLOBAL_UNIT_ASSIGNED_CONTEXT ( ( #13181, #30262, #12 ) ) REPRESENTATION_CONTEXT ( 'NONE', 'WORKASPACE' ) );
#32894=FACE_OUTER_BOUND ( 'NONE', #19683, .T. ) ;
#32895=CARTESIAN_POINT ( 'NONE',  ( -3.799999999999999822, 0.000000000000000000, -39.50000000000000711 ) ) ;
#32896=DIRECTION ( 'NONE',  ( 0.000000000000000000, 0.000000000000000000, -1.000000000000000000 ) ) ;
#32948=DIRECTION ( 'NONE',  ( -1.000000000000000000, 0.000000000000000000, 0.000000000000000000 ) ) ;
#32961=SURFACE_STYLE_FILL_AREA ( #21962 ) ;
#32979=PRESENTATION_STYLE_ASSIGNMENT (( #22158 ) ) ;
#33142=AXIS2_PLACEMENT_3D ( 'NONE', #21629, #32635, #25057 ) ;
#33161=DIRECTION ( 'NONE',  ( -1.000000000000000000, 0.000000000000000000, 0.000000000000000000 ) ) ;
#33198=CARTESIAN_POINT ( 'NONE',  ( 4.000000000000000000, 4.898587196589412829E-16, 55.00000000000000000 ) ) ;
#33252=CARTESIAN_POINT ( 'NONE',  ( -4.000000000000000000, 0.000000000000000000, -39.50000000000000711 ) ) ;
#33294=DIRECTION ( 'NONE',  ( -1.000000000000000000, 0.000000000000000000, 0.000000000000000000 ) ) ;
#33325=CIRCLE ( 'NONE', #13221, 3.799999999999999822 ) ;
#33650=FILL_AREA_STYLE_COLOUR ( '', #13919 ) ;
#33692=DIRECTION ( 'NONE',  ( 0.000000000000000000, 0.000000000000000000, -1.000000000000000000 ) ) ;
#33715=DIRECTION ( 'NONE',  ( 0.000000000000000000, 0.000000000000000000, -1.000000000000000000 ) ) ;
#33740=VECTOR ( 'NONE', #8346, 1000.000000000000000 ) ;
#33742=SHAPE_REPRESENTATION ( 'shaft1', ( #21307 ), #32890 ) ;
#33752=ORIENTED_EDGE ( 'NONE', *, *, #30275, .T. ) ;
#33758=ADVANCED_FACE ( 'NONE', ( #1782 ), #6284, .T. ) ;
#33776=EDGE_CURVE ( 'NONE', #17076, #34725, #4676, .T. ) ;
#33826=VERTEX_POINT ( 'NONE', #28787 ) ;
#33871=CYLINDRICAL_SURFACE ( 'NONE', #18763, 4.000000000000000000 ) ;
#33894=VERTEX_POINT ( 'NONE', #20475 ) ;
#33922=EDGE_LOOP ( 'NONE', ( #2061, #19947 ) ) ;
#33943=AXIS2_PLACEMENT_3D ( 'NONE', #9832, #23333, #29108 ) ;
#33972=ADVANCED_FACE ( 'NONE', ( #24808 ), #18676, .T. ) ;
#34006=ORIENTED_EDGE ( 'NONE', *, *, #14126, .T. ) ;
#34046=AXIS2_PLACEMENT_3D ( 'NONE', #13103, #4818, #32514 ) ;
#34115=DIRECTION ( 'NONE',  ( 0.000000000000000000, 0.000000000000000000, -1.000000000000000000 ) ) ;
#34189=ORIENTED_EDGE ( 'NONE', *, *, #20623, .T. ) ;
#34193=ORIENTED_EDGE ( 'NONE', *, *, #18522, .T. ) ;
#34219=CLOSED_SHELL ( 'NONE', ( #10395, #21163, #33758, #18779, #33972, #6306, #28042, #5618, #9087, #35607, #29972, #13933, #11175, #13229, #6925, #5815, #11281, #14154, #24855, #19193, #30803, #31498, #22209, #35509, #11102, #15736, #5482, #17576 ) ) ;
#34271=DIRECTION ( 'NONE',  ( 0.000000000000000000, 0.000000000000000000, -1.000000000000000000 ) ) ;
#34466=AXIS2_PLACEMENT_3D ( 'NONE', #1852, #31554, #1132 ) ;
#34608=EDGE_CURVE ( 'NONE', #485, #27576, #32551, .T. ) ;
#34645=ORIENTED_EDGE ( 'NONE', *, *, #27146, .T. ) ;
#34684=ORIENTED_EDGE ( 'NONE', *, *, #1380, .F. ) ;
#34690=CARTESIAN_POINT ( 'NONE',  ( 0.000000000000000000, 0.000000000000000000, -49.10000000000000142 ) ) ;
#34725=VERTEX_POINT ( 'NONE', #28520 ) ;
#34769=AXIS2_PLACEMENT_3D ( 'NONE', #4167, #23591, #31157 ) ;
#34774=CIRCLE ( 'NONE', #6030, 4.000000000000000000 ) ;
#34889=EDGE_LOOP ( 'NONE', ( #17257, #8744 ) ) ;
#34895=DIRECTION ( 'NONE',  ( 0.000000000000000000, 0.000000000000000000, -1.000000000000000000 ) ) ;
#34959=DIRECTION ( 'NONE',  ( -1.000000000000000000, 0.000000000000000000, 0.000000000000000000 ) ) ;
#35111=CIRCLE ( 'NONE', #21276, 3.799999999999999822 ) ;
#35166=EDGE_CURVE ( 'NONE', #33894, #27904, #8448, .T. ) ;
#35212=ORIENTED_EDGE ( 'NONE', *, *, #23108, .T. ) ;
#35326=EDGE_LOOP ( 'NONE', ( #8644, #21644, #20847, #26092 ) ) ;
#35363=DIRECTION ( 'NONE',  ( 0.000000000000000000, 0.000000000000000000, -1.000000000000000000 ) ) ;
#35428=ORIENTED_EDGE ( 'NONE', *, *, #10154, .T. ) ;
#35432=EDGE_CURVE ( 'NONE', #16603, #31617, #28573, .T. ) ;
#35433=FACE_OUTER_BOUND ( 'NONE', #17104, .T. ) ;
#35441=( GEOMETRIC_REPRESENTATION_CONTEXT ( 3 ) GLOBAL_UNCERTAINTY_ASSIGNED_CONTEXT ( ( #1006 ) ) GLOBAL_UNIT_ASSIGNED_CONTEXT ( ( #14051, #22676, #11017 ) ) REPRESENTATION_CONTEXT ( 'NONE', 'WORKASPACE' ) );
#35509=ADVANCED_FACE ( 'NONE', ( #5596 ), #24677, .T. ) ;
#35575=EDGE_CURVE ( 'NONE', #30211, #8680, #23157, .T. ) ;
#35581=EDGE_LOOP ( 'NONE', ( #11927, #11725, #9899, #13830 ) ) ;
#35603=CARTESIAN_POINT ( 'NONE',  ( 0.000000000000000000, 0.000000000000000000, 55.00000000000000000 ) ) ;
#35607=ADVANCED_FACE ( 'NONE', ( #31977 ), #12903, .T. ) ;
ENDSEC;
END-ISO-10303-21;
